ISO-10303-21;
HEADER;
/* Generated by software containing ST-Developer
 * from STEP Tools, Inc. (www.steptools.com) 
 */

FILE_DESCRIPTION(
/* description */ ('PAT-091'),
/* implementation_level */ '2;1');

FILE_NAME(
/* name */ 'Centre bearing retainer (1).step',
/* time_stamp */ '2026-10-27T15:34:44-07:00',
/* author */ (''),
/* organization */ (''),
/* preprocessor_version */ 'ST-DEVELOPER v20.2',
/* originating_system */ 'Autodesk Translation Framework v15.17.0.0',
/* authorisation */ '');

FILE_SCHEMA (('AUTOMOTIVE_DESIGN { 1 0 10303 214 3 1 1 }'));
ENDSEC;

DATA;
#10=MECHANICAL_DESIGN_GEOMETRIC_PRESENTATION_REPRESENTATION('',(#1052),#25100);
#832=SHAPE_REPRESENTATION_RELATIONSHIP('SRR','None',#25599,#942);
#942=ADVANCED_BREP_SHAPE_REPRESENTATION('',(#1173),#25069);
#1052=STYLED_ITEM('',(#26191),#1173);
#1173=MANIFOLD_SOLID_BREP('Body1',#13332);
#1557=FACE_BOUND('',#3833,.T.);
#1558=FACE_BOUND('',#3834,.T.);
#1559=FACE_BOUND('',#3835,.T.);
#1560=FACE_BOUND('',#3836,.T.);
#1561=FACE_BOUND('',#3837,.T.);
#1562=FACE_BOUND('',#3839,.T.);
#1563=FACE_BOUND('',#3840,.T.);
#1564=FACE_BOUND('',#3841,.T.);
#1565=FACE_BOUND('',#3842,.T.);
#1566=FACE_BOUND('',#3843,.T.);
#1972=PLANE('',#15910);
#1973=PLANE('',#15911);
#2666=FACE_OUTER_BOUND('',#3826,.T.);
#2667=FACE_OUTER_BOUND('',#3827,.T.);
#2668=FACE_OUTER_BOUND('',#3828,.T.);
#2669=FACE_OUTER_BOUND('',#3829,.T.);
#2670=FACE_OUTER_BOUND('',#3830,.T.);
#2671=FACE_OUTER_BOUND('',#3831,.T.);
#2672=FACE_OUTER_BOUND('',#3832,.T.);
#2673=FACE_OUTER_BOUND('',#3838,.T.);
#3826=EDGE_LOOP('',(#11342,#11343,#11344,#11345));
#3827=EDGE_LOOP('',(#11346,#11347,#11348,#11349));
#3828=EDGE_LOOP('',(#11350,#11351,#11352,#11353));
#3829=EDGE_LOOP('',(#11354,#11355,#11356,#11357));
#3830=EDGE_LOOP('',(#11358,#11359,#11360,#11361));
#3831=EDGE_LOOP('',(#11362,#11363,#11364,#11365));
#3832=EDGE_LOOP('',(#11366));
#3833=EDGE_LOOP('',(#11367));
#3834=EDGE_LOOP('',(#11368));
#3835=EDGE_LOOP('',(#11369));
#3836=EDGE_LOOP('',(#11370));
#3837=EDGE_LOOP('',(#11371));
#3838=EDGE_LOOP('',(#11372));
#3839=EDGE_LOOP('',(#11373));
#3840=EDGE_LOOP('',(#11374));
#3841=EDGE_LOOP('',(#11375));
#3842=EDGE_LOOP('',(#11376));
#3843=EDGE_LOOP('',(#11377));
#4765=LINE('',#23768,#5505);
#4766=LINE('',#23774,#5506);
#4767=LINE('',#23780,#5507);
#4768=LINE('',#23786,#5508);
#4769=LINE('',#23792,#5509);
#4770=LINE('',#23798,#5510);
#5505=VECTOR('',#19727,0.225000000000001);
#5506=VECTOR('',#19734,0.225000000000001);
#5507=VECTOR('',#19741,0.225000000000001);
#5508=VECTOR('',#19748,0.225000000000001);
#5509=VECTOR('',#19755,1.02);
#5510=VECTOR('',#19762,2.2);
#6144=CIRCLE('',#15893,0.225000000000001);
#6145=CIRCLE('',#15894,0.225000000000001);
#6146=CIRCLE('',#15896,0.225000000000001);
#6147=CIRCLE('',#15897,0.225000000000001);
#6148=CIRCLE('',#15899,0.225000000000001);
#6149=CIRCLE('',#15900,0.225000000000001);
#6150=CIRCLE('',#15902,0.225000000000001);
#6151=CIRCLE('',#15903,0.225000000000001);
#6152=CIRCLE('',#15905,1.02);
#6153=CIRCLE('',#15906,1.02);
#6154=CIRCLE('',#15908,2.2);
#6155=CIRCLE('',#15909,2.2);
#7169=VERTEX_POINT('',#23765);
#7170=VERTEX_POINT('',#23767);
#7171=VERTEX_POINT('',#23771);
#7172=VERTEX_POINT('',#23773);
#7173=VERTEX_POINT('',#23777);
#7174=VERTEX_POINT('',#23779);
#7175=VERTEX_POINT('',#23783);
#7176=VERTEX_POINT('',#23785);
#7177=VERTEX_POINT('',#23789);
#7178=VERTEX_POINT('',#23791);
#7179=VERTEX_POINT('',#23795);
#7180=VERTEX_POINT('',#23797);
#8606=EDGE_CURVE('',#7169,#7169,#6144,.T.);
#8607=EDGE_CURVE('',#7169,#7170,#4765,.T.);
#8608=EDGE_CURVE('',#7170,#7170,#6145,.T.);
#8609=EDGE_CURVE('',#7171,#7171,#6146,.T.);
#8610=EDGE_CURVE('',#7171,#7172,#4766,.T.);
#8611=EDGE_CURVE('',#7172,#7172,#6147,.T.);
#8612=EDGE_CURVE('',#7173,#7173,#6148,.T.);
#8613=EDGE_CURVE('',#7173,#7174,#4767,.T.);
#8614=EDGE_CURVE('',#7174,#7174,#6149,.T.);
#8615=EDGE_CURVE('',#7175,#7175,#6150,.T.);
#8616=EDGE_CURVE('',#7175,#7176,#4768,.T.);
#8617=EDGE_CURVE('',#7176,#7176,#6151,.T.);
#8618=EDGE_CURVE('',#7177,#7177,#6152,.T.);
#8619=EDGE_CURVE('',#7177,#7178,#4769,.T.);
#8620=EDGE_CURVE('',#7178,#7178,#6153,.T.);
#8621=EDGE_CURVE('',#7179,#7179,#6154,.T.);
#8622=EDGE_CURVE('',#7179,#7180,#4770,.T.);
#8623=EDGE_CURVE('',#7180,#7180,#6155,.T.);
#11342=ORIENTED_EDGE('',*,*,#8606,.F.);
#11343=ORIENTED_EDGE('',*,*,#8607,.T.);
#11344=ORIENTED_EDGE('',*,*,#8608,.F.);
#11345=ORIENTED_EDGE('',*,*,#8607,.F.);
#11346=ORIENTED_EDGE('',*,*,#8609,.F.);
#11347=ORIENTED_EDGE('',*,*,#8610,.T.);
#11348=ORIENTED_EDGE('',*,*,#8611,.F.);
#11349=ORIENTED_EDGE('',*,*,#8610,.F.);
#11350=ORIENTED_EDGE('',*,*,#8612,.F.);
#11351=ORIENTED_EDGE('',*,*,#8613,.T.);
#11352=ORIENTED_EDGE('',*,*,#8614,.F.);
#11353=ORIENTED_EDGE('',*,*,#8613,.F.);
#11354=ORIENTED_EDGE('',*,*,#8615,.F.);
#11355=ORIENTED_EDGE('',*,*,#8616,.T.);
#11356=ORIENTED_EDGE('',*,*,#8617,.F.);
#11357=ORIENTED_EDGE('',*,*,#8616,.F.);
#11358=ORIENTED_EDGE('',*,*,#8618,.F.);
#11359=ORIENTED_EDGE('',*,*,#8619,.T.);
#11360=ORIENTED_EDGE('',*,*,#8620,.T.);
#11361=ORIENTED_EDGE('',*,*,#8619,.F.);
#11362=ORIENTED_EDGE('',*,*,#8621,.F.);
#11363=ORIENTED_EDGE('',*,*,#8622,.T.);
#11364=ORIENTED_EDGE('',*,*,#8623,.T.);
#11365=ORIENTED_EDGE('',*,*,#8622,.F.);
#11366=ORIENTED_EDGE('',*,*,#8621,.T.);
#11367=ORIENTED_EDGE('',*,*,#8618,.T.);
#11368=ORIENTED_EDGE('',*,*,#8617,.T.);
#11369=ORIENTED_EDGE('',*,*,#8614,.T.);
#11370=ORIENTED_EDGE('',*,*,#8611,.T.);
#11371=ORIENTED_EDGE('',*,*,#8608,.T.);
#11372=ORIENTED_EDGE('',*,*,#8623,.F.);
#11373=ORIENTED_EDGE('',*,*,#8620,.F.);
#11374=ORIENTED_EDGE('',*,*,#8615,.T.);
#11375=ORIENTED_EDGE('',*,*,#8612,.T.);
#11376=ORIENTED_EDGE('',*,*,#8609,.T.);
#11377=ORIENTED_EDGE('',*,*,#8606,.T.);
#12333=CYLINDRICAL_SURFACE('',#15892,0.225000000000001);
#12334=CYLINDRICAL_SURFACE('',#15895,0.225000000000001);
#12335=CYLINDRICAL_SURFACE('',#15898,0.225000000000001);
#12336=CYLINDRICAL_SURFACE('',#15901,0.225000000000001);
#12337=CYLINDRICAL_SURFACE('',#15904,1.02);
#12338=CYLINDRICAL_SURFACE('',#15907,2.2);
#13033=ADVANCED_FACE('',(#2666),#12333,.F.);
#13034=ADVANCED_FACE('',(#2667),#12334,.F.);
#13035=ADVANCED_FACE('',(#2668),#12335,.F.);
#13036=ADVANCED_FACE('',(#2669),#12336,.F.);
#13037=ADVANCED_FACE('',(#2670),#12337,.F.);
#13038=ADVANCED_FACE('',(#2671),#12338,.T.);
#13039=ADVANCED_FACE('',(#2672,#1557,#1558,#1559,#1560,#1561),#1972,.T.);
#13040=ADVANCED_FACE('',(#2673,#1562,#1563,#1564,#1565,#1566),#1973,.F.);
#13332=CLOSED_SHELL('',(#13033,#13034,#13035,#13036,#13037,#13038,#13039,
#13040));
#15891=AXIS2_PLACEMENT_3D('',#23763,#19721,#19722);
#15892=AXIS2_PLACEMENT_3D('',#23764,#19723,#19724);
#15893=AXIS2_PLACEMENT_3D('',#23766,#19725,#19726);
#15894=AXIS2_PLACEMENT_3D('',#23769,#19728,#19729);
#15895=AXIS2_PLACEMENT_3D('',#23770,#19730,#19731);
#15896=AXIS2_PLACEMENT_3D('',#23772,#19732,#19733);
#15897=AXIS2_PLACEMENT_3D('',#23775,#19735,#19736);
#15898=AXIS2_PLACEMENT_3D('',#23776,#19737,#19738);
#15899=AXIS2_PLACEMENT_3D('',#23778,#19739,#19740);
#15900=AXIS2_PLACEMENT_3D('',#23781,#19742,#19743);
#15901=AXIS2_PLACEMENT_3D('',#23782,#19744,#19745);
#15902=AXIS2_PLACEMENT_3D('',#23784,#19746,#19747);
#15903=AXIS2_PLACEMENT_3D('',#23787,#19749,#19750);
#15904=AXIS2_PLACEMENT_3D('',#23788,#19751,#19752);
#15905=AXIS2_PLACEMENT_3D('',#23790,#19753,#19754);
#15906=AXIS2_PLACEMENT_3D('',#23793,#19756,#19757);
#15907=AXIS2_PLACEMENT_3D('',#23794,#19758,#19759);
#15908=AXIS2_PLACEMENT_3D('',#23796,#19760,#19761);
#15909=AXIS2_PLACEMENT_3D('',#23799,#19763,#19764);
#15910=AXIS2_PLACEMENT_3D('',#23800,#19765,#19766);
#15911=AXIS2_PLACEMENT_3D('',#23801,#19767,#19768);
#19721=DIRECTION('axis',(0.,0.,1.));
#19722=DIRECTION('refdir',(1.,0.,0.));
#19723=DIRECTION('center_axis',(0.,1.,0.));
#19724=DIRECTION('ref_axis',(1.,0.,0.));
#19725=DIRECTION('center_axis',(0.,1.,0.));
#19726=DIRECTION('ref_axis',(1.,0.,0.));
#19727=DIRECTION('',(0.,1.,0.));
#19728=DIRECTION('center_axis',(0.,-1.,0.));
#19729=DIRECTION('ref_axis',(1.,0.,0.));
#19730=DIRECTION('center_axis',(0.,1.,0.));
#19731=DIRECTION('ref_axis',(1.,0.,0.));
#19732=DIRECTION('center_axis',(0.,1.,0.));
#19733=DIRECTION('ref_axis',(1.,0.,0.));
#19734=DIRECTION('',(0.,1.,0.));
#19735=DIRECTION('center_axis',(0.,-1.,0.));
#19736=DIRECTION('ref_axis',(1.,0.,0.));
#19737=DIRECTION('center_axis',(0.,1.,0.));
#19738=DIRECTION('ref_axis',(1.,0.,0.));
#19739=DIRECTION('center_axis',(0.,1.,0.));
#19740=DIRECTION('ref_axis',(1.,0.,0.));
#19741=DIRECTION('',(0.,1.,0.));
#19742=DIRECTION('center_axis',(0.,-1.,0.));
#19743=DIRECTION('ref_axis',(1.,0.,0.));
#19744=DIRECTION('center_axis',(0.,1.,0.));
#19745=DIRECTION('ref_axis',(1.,0.,0.));
#19746=DIRECTION('center_axis',(0.,1.,0.));
#19747=DIRECTION('ref_axis',(1.,0.,0.));
#19748=DIRECTION('',(0.,1.,0.));
#19749=DIRECTION('center_axis',(0.,-1.,0.));
#19750=DIRECTION('ref_axis',(1.,0.,0.));
#19751=DIRECTION('center_axis',(0.,1.,0.));
#19752=DIRECTION('ref_axis',(1.,0.,0.));
#19753=DIRECTION('center_axis',(0.,-1.,0.));
#19754=DIRECTION('ref_axis',(1.,0.,0.));
#19755=DIRECTION('',(0.,-1.,0.));
#19756=DIRECTION('center_axis',(0.,-1.,0.));
#19757=DIRECTION('ref_axis',(1.,0.,0.));
#19758=DIRECTION('center_axis',(0.,1.,0.));
#19759=DIRECTION('ref_axis',(1.,0.,0.));
#19760=DIRECTION('center_axis',(0.,1.,0.));
#19761=DIRECTION('ref_axis',(1.,0.,0.));
#19762=DIRECTION('',(0.,-1.,0.));
#19763=DIRECTION('center_axis',(0.,1.,0.));
#19764=DIRECTION('ref_axis',(1.,0.,0.));
#19765=DIRECTION('center_axis',(0.,1.,0.));
#19766=DIRECTION('ref_axis',(1.,0.,0.));
#19767=DIRECTION('center_axis',(0.,1.,0.));
#19768=DIRECTION('ref_axis',(1.,0.,0.));
#23763=CARTESIAN_POINT('',(0.,0.,0.));
#23764=CARTESIAN_POINT('Origin',(18.056769185842,-4.6,6.69185245480489));
#23765=CARTESIAN_POINT('',(17.831769185842,-4.5,6.69185245480489));
#23766=CARTESIAN_POINT('Origin',(18.056769185842,-4.5,6.69185245480489));
#23767=CARTESIAN_POINT('',(17.831769185842,-4.2,6.69185245480489));
#23768=CARTESIAN_POINT('',(17.831769185842,-4.6,6.69185245480489));
#23769=CARTESIAN_POINT('Origin',(18.056769185842,-4.2,6.69185245480489));
#23770=CARTESIAN_POINT('Origin',(18.056769185842,-4.6,9.30814754519511));
#23771=CARTESIAN_POINT('',(17.831769185842,-4.5,9.30814754519511));
#23772=CARTESIAN_POINT('Origin',(18.056769185842,-4.5,9.30814754519511));
#23773=CARTESIAN_POINT('',(17.831769185842,-4.2,9.30814754519511));
#23774=CARTESIAN_POINT('',(17.831769185842,-4.6,9.30814754519511));
#23775=CARTESIAN_POINT('Origin',(18.056769185842,-4.2,9.30814754519511));
#23776=CARTESIAN_POINT('Origin',(20.6730642762322,-4.6,9.30814754519511));
#23777=CARTESIAN_POINT('',(20.4480642762322,-4.5,9.30814754519511));
#23778=CARTESIAN_POINT('Origin',(20.6730642762322,-4.5,9.30814754519511));
#23779=CARTESIAN_POINT('',(20.4480642762322,-4.2,9.30814754519511));
#23780=CARTESIAN_POINT('',(20.4480642762322,-4.6,9.30814754519511));
#23781=CARTESIAN_POINT('Origin',(20.6730642762322,-4.2,9.30814754519511));
#23782=CARTESIAN_POINT('Origin',(20.6730642762322,-4.6,6.69185245480489));
#23783=CARTESIAN_POINT('',(20.4480642762322,-4.5,6.69185245480489));
#23784=CARTESIAN_POINT('Origin',(20.6730642762322,-4.5,6.69185245480489));
#23785=CARTESIAN_POINT('',(20.4480642762322,-4.2,6.69185245480489));
#23786=CARTESIAN_POINT('',(20.4480642762322,-4.6,6.69185245480489));
#23787=CARTESIAN_POINT('Origin',(20.6730642762322,-4.2,6.69185245480489));
#23788=CARTESIAN_POINT('Origin',(19.3649167310371,-4.5,8.));
#23789=CARTESIAN_POINT('',(18.3449167310371,-4.2,8.));
#23790=CARTESIAN_POINT('Origin',(19.3649167310371,-4.2,8.));
#23791=CARTESIAN_POINT('',(18.3449167310371,-4.5,8.));
#23792=CARTESIAN_POINT('',(18.3449167310371,-4.5,8.));
#23793=CARTESIAN_POINT('Origin',(19.3649167310371,-4.5,8.));
#23794=CARTESIAN_POINT('Origin',(19.3649167310371,-4.5,8.));
#23795=CARTESIAN_POINT('',(17.1649167310371,-4.2,8.));
#23796=CARTESIAN_POINT('Origin',(19.3649167310371,-4.2,8.));
#23797=CARTESIAN_POINT('',(17.1649167310371,-4.5,8.));
#23798=CARTESIAN_POINT('',(17.1649167310371,-4.5,8.));
#23799=CARTESIAN_POINT('Origin',(19.3649167310371,-4.5,8.));
#23800=CARTESIAN_POINT('Origin',(19.3649167310371,-4.2,8.));
#23801=CARTESIAN_POINT('Origin',(19.3649167310371,-4.5,8.));
#24948=UNCERTAINTY_MEASURE_WITH_UNIT(LENGTH_MEASURE(0.001),#25101,
'DISTANCE_ACCURACY_VALUE',
'Maximum model space distance between geometric entities at asserted c
onnectivities');
#24979=UNCERTAINTY_MEASURE_WITH_UNIT(LENGTH_MEASURE(0.001),#25101,
'DISTANCE_ACCURACY_VALUE',
'Maximum model space distance between geometric entities at asserted c
onnectivities');
#25069=(
GEOMETRIC_REPRESENTATION_CONTEXT(3)
GLOBAL_UNCERTAINTY_ASSIGNED_CONTEXT((#24948))
GLOBAL_UNIT_ASSIGNED_CONTEXT((#25101,#25103,#25104))
REPRESENTATION_CONTEXT('','3D')
);
#25100=(
GEOMETRIC_REPRESENTATION_CONTEXT(3)
GLOBAL_UNCERTAINTY_ASSIGNED_CONTEXT((#24979))
GLOBAL_UNIT_ASSIGNED_CONTEXT((#25101,#25103,#25104))
REPRESENTATION_CONTEXT('','3D')
);
#25101=(
LENGTH_UNIT()
NAMED_UNIT(*)
SI_UNIT(.CENTI.,.METRE.)
);
#25103=(
NAMED_UNIT(*)
PLANE_ANGLE_UNIT()
SI_UNIT($,.RADIAN.)
);
#25104=(
NAMED_UNIT(*)
SI_UNIT($,.STERADIAN.)
SOLID_ANGLE_UNIT()
);
#25194=SHAPE_DEFINITION_REPRESENTATION(#25388,#25599);
#25388=PRODUCT_DEFINITION_SHAPE('',$,#25720);
#25599=SHAPE_REPRESENTATION('',(#15891),#25069);
#25630=PRODUCT_DEFINITION_CONTEXT('part definition',#25992,'design');
#25720=PRODUCT_DEFINITION('Centre bearing retainer (1)',
'Centre bearing retainer (1)',#25840,#25630);
#25840=PRODUCT_DEFINITION_FORMATION('',$,#26083);
#25992=APPLICATION_CONTEXT(
'Core Data for Automotive Mechanical Design Process');
#25993=PRODUCT_CONTEXT('part definition',#25992,'mechanical');
#26083=PRODUCT('Centre bearing retainer (1)',
'Centre bearing retainer (1)','Centre bearing retainer (1)',(#25993));
#26185=COLOUR_RGB('Grey',0.48,0.52,0.57);
#26186=FILL_AREA_STYLE_COLOUR('',#26185);
#26187=FILL_AREA_STYLE('',(#26186));
#26188=SURFACE_STYLE_FILL_AREA(#26187);
#26189=SURFACE_SIDE_STYLE('',(#26188));
#26190=SURFACE_STYLE_USAGE(.BOTH.,#26189);
#26191=PRESENTATION_STYLE_ASSIGNMENT((#26190));
ENDSEC;
END-ISO-10303-21;
